ISO-10303-21;
HEADER;
/* Generated by software containing ST-Developer
 * from STEP Tools, Inc. (www.steptools.com) 
 */

FILE_DESCRIPTION(
/* description */ (''),
/* implementation_level */ '2;1');

FILE_NAME(
/* name */ 'Bottom_Block_01.step',
/* time_stamp */ '2026-10-23T22:30:33+06:00',
/* author */ (''),
/* organization */ (''),
/* preprocessor_version */ 'ST-DEVELOPER v20.2',
/* originating_system */ 'Autodesk Translation Framework v15.15.0.0',
/* authorisation */ '');

FILE_SCHEMA (('AUTOMOTIVE_DESIGN { 1 0 10303 214 3 1 1 }'));
ENDSEC;

DATA;
#10=MECHANICAL_DESIGN_GEOMETRIC_PRESENTATION_REPRESENTATION('',(#238),#10131);
#75=ELLIPSE('',#6175,1.08239220029239,1.);
#76=ELLIPSE('',#6176,1.08239220029239,1.);
#77=ELLIPSE('',#6178,1.08239220029239,1.);
#78=ELLIPSE('',#6179,1.08239220029239,1.);
#79=ELLIPSE('',#6181,1.08239220029239,1.);
#80=ELLIPSE('',#6183,1.0823922002924,1.);
#81=ELLIPSE('',#6185,1.08239220029239,1.);
#82=ELLIPSE('',#6187,1.0823922002924,1.);
#83=ELLIPSE('',#6189,1.08239220029239,1.);
#84=ELLIPSE('',#6191,1.0823922002924,1.);
#85=ELLIPSE('',#6193,1.08239220029239,1.);
#86=ELLIPSE('',#6195,1.0823922002924,1.);
#87=ELLIPSE('',#6206,1.08239220029239,1.);
#88=ELLIPSE('',#6207,1.0823922002924,1.);
#89=ELLIPSE('',#6209,1.08239220029239,1.);
#90=ELLIPSE('',#6211,1.0823922002924,1.);
#91=ELLIPSE('',#6213,1.08239220029239,1.);
#92=ELLIPSE('',#6215,1.0823922002924,1.);
#93=ELLIPSE('',#6217,1.08239220029239,1.);
#94=ELLIPSE('',#6219,1.0823922002924,1.);
#95=ELLIPSE('',#6221,1.08239220029239,1.);
#96=ELLIPSE('',#6223,1.0823922002924,1.);
#97=ELLIPSE('',#6225,1.08239220029239,1.);
#98=ELLIPSE('',#6227,1.08239220029239,1.);
#218=SHAPE_REPRESENTATION_RELATIONSHIP('SRR','None',#10172,#228);
#228=ADVANCED_BREP_SHAPE_REPRESENTATION('',(#248),#10124);
#238=STYLED_ITEM('',(#10247),#248);
#248=MANIFOLD_SOLID_BREP('Bottom_Block_01',#5882);
#374=PLANE('',#6198);
#375=PLANE('',#6199);
#376=PLANE('',#6200);
#377=PLANE('',#6201);
#378=PLANE('',#6202);
#379=PLANE('',#6203);
#380=PLANE('',#6204);
#381=PLANE('',#6229);
#382=PLANE('',#6230);
#383=PLANE('',#6231);
#384=PLANE('',#6232);
#385=PLANE('',#6233);
#386=PLANE('',#6234);
#387=PLANE('',#6235);
#566=FACE_OUTER_BOUND('',#941,.T.);
#567=FACE_OUTER_BOUND('',#942,.T.);
#568=FACE_OUTER_BOUND('',#943,.T.);
#569=FACE_OUTER_BOUND('',#944,.T.);
#570=FACE_OUTER_BOUND('',#945,.T.);
#571=FACE_OUTER_BOUND('',#946,.T.);
#572=FACE_OUTER_BOUND('',#947,.T.);
#573=FACE_OUTER_BOUND('',#948,.T.);
#574=FACE_OUTER_BOUND('',#949,.T.);
#575=FACE_OUTER_BOUND('',#950,.T.);
#576=FACE_OUTER_BOUND('',#951,.T.);
#577=FACE_OUTER_BOUND('',#952,.T.);
#578=FACE_OUTER_BOUND('',#953,.T.);
#579=FACE_OUTER_BOUND('',#954,.T.);
#580=FACE_OUTER_BOUND('',#955,.T.);
#581=FACE_OUTER_BOUND('',#956,.T.);
#582=FACE_OUTER_BOUND('',#957,.T.);
#583=FACE_OUTER_BOUND('',#958,.T.);
#584=FACE_OUTER_BOUND('',#959,.T.);
#585=FACE_OUTER_BOUND('',#960,.T.);
#586=FACE_OUTER_BOUND('',#961,.T.);
#587=FACE_OUTER_BOUND('',#962,.T.);
#588=FACE_OUTER_BOUND('',#963,.T.);
#589=FACE_OUTER_BOUND('',#964,.T.);
#590=FACE_OUTER_BOUND('',#965,.T.);
#591=FACE_OUTER_BOUND('',#966,.T.);
#592=FACE_OUTER_BOUND('',#967,.T.);
#593=FACE_OUTER_BOUND('',#968,.T.);
#594=FACE_OUTER_BOUND('',#969,.T.);
#595=FACE_OUTER_BOUND('',#970,.T.);
#596=FACE_OUTER_BOUND('',#971,.T.);
#597=FACE_OUTER_BOUND('',#972,.T.);
#598=FACE_OUTER_BOUND('',#973,.T.);
#599=FACE_OUTER_BOUND('',#974,.T.);
#600=FACE_OUTER_BOUND('',#975,.T.);
#601=FACE_OUTER_BOUND('',#976,.T.);
#602=FACE_OUTER_BOUND('',#977,.T.);
#603=FACE_OUTER_BOUND('',#978,.T.);
#941=EDGE_LOOP('',(#4194,#4195,#4196,#4197));
#942=EDGE_LOOP('',(#4198,#4199,#4200,#4201));
#943=EDGE_LOOP('',(#4202,#4203,#4204,#4205));
#944=EDGE_LOOP('',(#4206,#4207,#4208,#4209));
#945=EDGE_LOOP('',(#4210,#4211,#4212,#4213));
#946=EDGE_LOOP('',(#4214,#4215,#4216,#4217));
#947=EDGE_LOOP('',(#4218,#4219,#4220,#4221));
#948=EDGE_LOOP('',(#4222,#4223,#4224,#4225));
#949=EDGE_LOOP('',(#4226,#4227,#4228,#4229));
#950=EDGE_LOOP('',(#4230,#4231,#4232,#4233));
#951=EDGE_LOOP('',(#4234,#4235,#4236,#4237));
#952=EDGE_LOOP('',(#4238,#4239,#4240,#4241));
#953=EDGE_LOOP('',(#4242,#4243,#4244,#4245));
#954=EDGE_LOOP('',(#4246,#4247,#4248,#4249));
#955=EDGE_LOOP('',(#4250,#4251,#4252,#4253));
#956=EDGE_LOOP('',(#4254,#4255,#4256,#4257));
#957=EDGE_LOOP('',(#4258,#4259,#4260,#4261));
#958=EDGE_LOOP('',(#4262,#4263,#4264,#4265));
#959=EDGE_LOOP('',(#4266,#4267,#4268,#4269,#4270,#4271,#4272,#4273,#4274,
#4275,#4276,#4277));
#960=EDGE_LOOP('',(#4278,#4279,#4280,#4281));
#961=EDGE_LOOP('',(#4282,#4283,#4284,#4285));
#962=EDGE_LOOP('',(#4286,#4287,#4288,#4289));
#963=EDGE_LOOP('',(#4290,#4291,#4292,#4293));
#964=EDGE_LOOP('',(#4294,#4295,#4296,#4297));
#965=EDGE_LOOP('',(#4298,#4299,#4300,#4301));
#966=EDGE_LOOP('',(#4302,#4303,#4304,#4305));
#967=EDGE_LOOP('',(#4306,#4307,#4308,#4309));
#968=EDGE_LOOP('',(#4310,#4311,#4312,#4313));
#969=EDGE_LOOP('',(#4314,#4315,#4316,#4317));
#970=EDGE_LOOP('',(#4318,#4319,#4320,#4321));
#971=EDGE_LOOP('',(#4322,#4323,#4324,#4325));
#972=EDGE_LOOP('',(#4326,#4327,#4328,#4329));
#973=EDGE_LOOP('',(#4330,#4331,#4332,#4333));
#974=EDGE_LOOP('',(#4334,#4335,#4336,#4337));
#975=EDGE_LOOP('',(#4338,#4339,#4340,#4341,#4342,#4343,#4344,#4345,#4346,
#4347,#4348,#4349));
#976=EDGE_LOOP('',(#4350,#4351,#4352,#4353));
#977=EDGE_LOOP('',(#4354,#4355,#4356,#4357));
#978=EDGE_LOOP('',(#4358,#4359,#4360,#4361));
#1399=LINE('',#8944,#1949);
#1400=LINE('',#8948,#1950);
#1401=LINE('',#8953,#1951);
#1402=LINE('',#8957,#1952);
#1403=LINE('',#8961,#1953);
#1404=LINE('',#8964,#1954);
#1405=LINE('',#8967,#1955);
#1406=LINE('',#8970,#1956);
#1407=LINE('',#8973,#1957);
#1408=LINE('',#8976,#1958);
#1409=LINE('',#8979,#1959);
#1410=LINE('',#8982,#1960);
#1411=LINE('',#8985,#1961);
#1412=LINE('',#8987,#1962);
#1413=LINE('',#8991,#1963);
#1414=LINE('',#8993,#1964);
#1415=LINE('',#8997,#1965);
#1416=LINE('',#8999,#1966);
#1417=LINE('',#9003,#1967);
#1418=LINE('',#9005,#1968);
#1419=LINE('',#9008,#1969);
#1420=LINE('',#9009,#1970);
#1421=LINE('',#9011,#1971);
#1422=LINE('',#9012,#1972);
#1423=LINE('',#9015,#1973);
#1424=LINE('',#9017,#1974);
#1425=LINE('',#9018,#1975);
#1426=LINE('',#9021,#1976);
#1427=LINE('',#9022,#1977);
#1428=LINE('',#9025,#1978);
#1429=LINE('',#9026,#1979);
#1430=LINE('',#9029,#1980);
#1431=LINE('',#9030,#1981);
#1432=LINE('',#9033,#1982);
#1433=LINE('',#9034,#1983);
#1434=LINE('',#9037,#1984);
#1435=LINE('',#9038,#1985);
#1436=LINE('',#9043,#1986);
#1437=LINE('',#9048,#1987);
#1438=LINE('',#9052,#1988);
#1439=LINE('',#9056,#1989);
#1440=LINE('',#9060,#1990);
#1441=LINE('',#9063,#1991);
#1442=LINE('',#9066,#1992);
#1443=LINE('',#9068,#1993);
#1444=LINE('',#9072,#1994);
#1445=LINE('',#9074,#1995);
#1446=LINE('',#9078,#1996);
#1447=LINE('',#9080,#1997);
#1448=LINE('',#9084,#1998);
#1449=LINE('',#9086,#1999);
#1450=LINE('',#9089,#2000);
#1451=LINE('',#9091,#2001);
#1452=LINE('',#9095,#2002);
#1453=LINE('',#9098,#2003);
#1454=LINE('',#9100,#2004);
#1455=LINE('',#9101,#2005);
#1456=LINE('',#9103,#2006);
#1457=LINE('',#9107,#2007);
#1458=LINE('',#9108,#2008);
#1949=VECTOR('',#7137,10.);
#1950=VECTOR('',#7140,10.);
#1951=VECTOR('',#7145,10.);
#1952=VECTOR('',#7148,10.);
#1953=VECTOR('',#7153,10.);
#1954=VECTOR('',#7156,10.);
#1955=VECTOR('',#7159,10.);
#1956=VECTOR('',#7162,10.);
#1957=VECTOR('',#7165,10.);
#1958=VECTOR('',#7168,10.);
#1959=VECTOR('',#7171,10.);
#1960=VECTOR('',#7174,10.);
#1961=VECTOR('',#7177,10.);
#1962=VECTOR('',#7178,10.);
#1963=VECTOR('',#7183,10.);
#1964=VECTOR('',#7184,10.);
#1965=VECTOR('',#7189,10.);
#1966=VECTOR('',#7190,10.);
#1967=VECTOR('',#7195,10.);
#1968=VECTOR('',#7196,10.);
#1969=VECTOR('',#7201,10.);
#1970=VECTOR('',#7202,10.);
#1971=VECTOR('',#7205,10.);
#1972=VECTOR('',#7206,10.);
#1973=VECTOR('',#7209,10.);
#1974=VECTOR('',#7210,10.);
#1975=VECTOR('',#7211,10.);
#1976=VECTOR('',#7214,10.);
#1977=VECTOR('',#7215,10.);
#1978=VECTOR('',#7218,10.);
#1979=VECTOR('',#7219,10.);
#1980=VECTOR('',#7222,10.);
#1981=VECTOR('',#7223,10.);
#1982=VECTOR('',#7226,10.);
#1983=VECTOR('',#7227,10.);
#1984=VECTOR('',#7230,10.);
#1985=VECTOR('',#7231,10.);
#1986=VECTOR('',#7236,10.);
#1987=VECTOR('',#7243,10.);
#1988=VECTOR('',#7248,10.);
#1989=VECTOR('',#7253,10.);
#1990=VECTOR('',#7258,10.);
#1991=VECTOR('',#7261,10.);
#1992=VECTOR('',#7264,10.);
#1993=VECTOR('',#7265,10.);
#1994=VECTOR('',#7270,10.);
#1995=VECTOR('',#7271,10.);
#1996=VECTOR('',#7276,10.);
#1997=VECTOR('',#7277,10.);
#1998=VECTOR('',#7282,10.);
#1999=VECTOR('',#7283,10.);
#2000=VECTOR('',#7288,10.);
#2001=VECTOR('',#7289,10.);
#2002=VECTOR('',#7294,10.);
#2003=VECTOR('',#7299,10.);
#2004=VECTOR('',#7302,10.);
#2005=VECTOR('',#7303,10.);
#2006=VECTOR('',#7306,10.);
#2007=VECTOR('',#7313,10.);
#2008=VECTOR('',#7314,10.);
#2576=VERTEX_POINT('',#8942);
#2577=VERTEX_POINT('',#8943);
#2578=VERTEX_POINT('',#8945);
#2579=VERTEX_POINT('',#8947);
#2580=VERTEX_POINT('',#8951);
#2581=VERTEX_POINT('',#8952);
#2582=VERTEX_POINT('',#8954);
#2583=VERTEX_POINT('',#8956);
#2584=VERTEX_POINT('',#8960);
#2585=VERTEX_POINT('',#8962);
#2586=VERTEX_POINT('',#8966);
#2587=VERTEX_POINT('',#8968);
#2588=VERTEX_POINT('',#8972);
#2589=VERTEX_POINT('',#8974);
#2590=VERTEX_POINT('',#8978);
#2591=VERTEX_POINT('',#8980);
#2592=VERTEX_POINT('',#8984);
#2593=VERTEX_POINT('',#8986);
#2594=VERTEX_POINT('',#8990);
#2595=VERTEX_POINT('',#8992);
#2596=VERTEX_POINT('',#8996);
#2597=VERTEX_POINT('',#8998);
#2598=VERTEX_POINT('',#9002);
#2599=VERTEX_POINT('',#9004);
#2600=VERTEX_POINT('',#9014);
#2601=VERTEX_POINT('',#9016);
#2602=VERTEX_POINT('',#9020);
#2603=VERTEX_POINT('',#9024);
#2604=VERTEX_POINT('',#9028);
#2605=VERTEX_POINT('',#9032);
#2606=VERTEX_POINT('',#9036);
#2607=VERTEX_POINT('',#9041);
#2608=VERTEX_POINT('',#9042);
#2609=VERTEX_POINT('',#9047);
#2610=VERTEX_POINT('',#9051);
#2611=VERTEX_POINT('',#9055);
#2612=VERTEX_POINT('',#9059);
#2613=VERTEX_POINT('',#9061);
#2614=VERTEX_POINT('',#9065);
#2615=VERTEX_POINT('',#9067);
#2616=VERTEX_POINT('',#9071);
#2617=VERTEX_POINT('',#9073);
#2618=VERTEX_POINT('',#9077);
#2619=VERTEX_POINT('',#9079);
#2620=VERTEX_POINT('',#9083);
#2621=VERTEX_POINT('',#9085);
#2622=VERTEX_POINT('',#9090);
#2623=VERTEX_POINT('',#9094);
#3149=EDGE_CURVE('',#2576,#2577,#1399,.T.);
#3150=EDGE_CURVE('',#2577,#2578,#75,.T.);
#3151=EDGE_CURVE('',#2578,#2579,#1400,.T.);
#3152=EDGE_CURVE('',#2579,#2576,#76,.T.);
#3153=EDGE_CURVE('',#2580,#2581,#1401,.T.);
#3154=EDGE_CURVE('',#2581,#2582,#77,.T.);
#3155=EDGE_CURVE('',#2582,#2583,#1402,.T.);
#3156=EDGE_CURVE('',#2583,#2580,#78,.T.);
#3157=EDGE_CURVE('',#2581,#2584,#1403,.T.);
#3158=EDGE_CURVE('',#2584,#2585,#79,.T.);
#3159=EDGE_CURVE('',#2585,#2582,#1404,.T.);
#3160=EDGE_CURVE('',#2584,#2586,#1405,.T.);
#3161=EDGE_CURVE('',#2586,#2587,#80,.T.);
#3162=EDGE_CURVE('',#2587,#2585,#1406,.T.);
#3163=EDGE_CURVE('',#2586,#2588,#1407,.T.);
#3164=EDGE_CURVE('',#2588,#2589,#81,.T.);
#3165=EDGE_CURVE('',#2589,#2587,#1408,.T.);
#3166=EDGE_CURVE('',#2588,#2590,#1409,.T.);
#3167=EDGE_CURVE('',#2590,#2591,#82,.T.);
#3168=EDGE_CURVE('',#2591,#2589,#1410,.T.);
#3169=EDGE_CURVE('',#2592,#2591,#1411,.T.);
#3170=EDGE_CURVE('',#2590,#2593,#1412,.T.);
#3171=EDGE_CURVE('',#2593,#2592,#83,.T.);
#3172=EDGE_CURVE('',#2594,#2592,#1413,.T.);
#3173=EDGE_CURVE('',#2593,#2595,#1414,.T.);
#3174=EDGE_CURVE('',#2595,#2594,#84,.T.);
#3175=EDGE_CURVE('',#2596,#2594,#1415,.T.);
#3176=EDGE_CURVE('',#2595,#2597,#1416,.T.);
#3177=EDGE_CURVE('',#2597,#2596,#85,.T.);
#3178=EDGE_CURVE('',#2598,#2596,#1417,.T.);
#3179=EDGE_CURVE('',#2597,#2599,#1418,.T.);
#3180=EDGE_CURVE('',#2599,#2598,#86,.T.);
#3181=EDGE_CURVE('',#2577,#2598,#1419,.T.);
#3182=EDGE_CURVE('',#2599,#2578,#1420,.T.);
#3183=EDGE_CURVE('',#2583,#2576,#1421,.T.);
#3184=EDGE_CURVE('',#2579,#2580,#1422,.T.);
#3185=EDGE_CURVE('',#2596,#2600,#1423,.T.);
#3186=EDGE_CURVE('',#2601,#2600,#1424,.T.);
#3187=EDGE_CURVE('',#2601,#2594,#1425,.T.);
#3188=EDGE_CURVE('',#2602,#2598,#1426,.T.);
#3189=EDGE_CURVE('',#2600,#2602,#1427,.T.);
#3190=EDGE_CURVE('',#2577,#2603,#1428,.T.);
#3191=EDGE_CURVE('',#2602,#2603,#1429,.T.);
#3192=EDGE_CURVE('',#2604,#2576,#1430,.T.);
#3193=EDGE_CURVE('',#2603,#2604,#1431,.T.);
#3194=EDGE_CURVE('',#2583,#2605,#1432,.T.);
#3195=EDGE_CURVE('',#2604,#2605,#1433,.T.);
#3196=EDGE_CURVE('',#2606,#2582,#1434,.T.);
#3197=EDGE_CURVE('',#2605,#2606,#1435,.T.);
#3198=EDGE_CURVE('',#2607,#2608,#1436,.T.);
#3199=EDGE_CURVE('',#2608,#2603,#87,.T.);
#3200=EDGE_CURVE('',#2607,#2604,#88,.T.);
#3201=EDGE_CURVE('',#2608,#2609,#1437,.T.);
#3202=EDGE_CURVE('',#2609,#2602,#89,.T.);
#3203=EDGE_CURVE('',#2609,#2610,#1438,.T.);
#3204=EDGE_CURVE('',#2610,#2600,#90,.T.);
#3205=EDGE_CURVE('',#2610,#2611,#1439,.T.);
#3206=EDGE_CURVE('',#2611,#2601,#91,.T.);
#3207=EDGE_CURVE('',#2611,#2612,#1440,.T.);
#3208=EDGE_CURVE('',#2612,#2613,#92,.T.);
#3209=EDGE_CURVE('',#2613,#2601,#1441,.T.);
#3210=EDGE_CURVE('',#2614,#2613,#1442,.T.);
#3211=EDGE_CURVE('',#2612,#2615,#1443,.T.);
#3212=EDGE_CURVE('',#2615,#2614,#93,.T.);
#3213=EDGE_CURVE('',#2616,#2614,#1444,.T.);
#3214=EDGE_CURVE('',#2615,#2617,#1445,.T.);
#3215=EDGE_CURVE('',#2617,#2616,#94,.T.);
#3216=EDGE_CURVE('',#2618,#2616,#1446,.T.);
#3217=EDGE_CURVE('',#2617,#2619,#1447,.T.);
#3218=EDGE_CURVE('',#2619,#2618,#95,.T.);
#3219=EDGE_CURVE('',#2620,#2618,#1448,.T.);
#3220=EDGE_CURVE('',#2619,#2621,#1449,.T.);
#3221=EDGE_CURVE('',#2621,#2620,#96,.T.);
#3222=EDGE_CURVE('',#2606,#2620,#1450,.T.);
#3223=EDGE_CURVE('',#2621,#2622,#1451,.T.);
#3224=EDGE_CURVE('',#2622,#2606,#97,.T.);
#3225=EDGE_CURVE('',#2622,#2623,#1452,.T.);
#3226=EDGE_CURVE('',#2623,#2605,#98,.T.);
#3227=EDGE_CURVE('',#2623,#2607,#1453,.T.);
#3228=EDGE_CURVE('',#2589,#2616,#1454,.T.);
#3229=EDGE_CURVE('',#2618,#2587,#1455,.T.);
#3230=EDGE_CURVE('',#2585,#2620,#1456,.T.);
#3231=EDGE_CURVE('',#2592,#2613,#1457,.T.);
#3232=EDGE_CURVE('',#2614,#2591,#1458,.T.);
#4194=ORIENTED_EDGE('',*,*,#3149,.T.);
#4195=ORIENTED_EDGE('',*,*,#3150,.T.);
#4196=ORIENTED_EDGE('',*,*,#3151,.T.);
#4197=ORIENTED_EDGE('',*,*,#3152,.T.);
#4198=ORIENTED_EDGE('',*,*,#3153,.T.);
#4199=ORIENTED_EDGE('',*,*,#3154,.T.);
#4200=ORIENTED_EDGE('',*,*,#3155,.T.);
#4201=ORIENTED_EDGE('',*,*,#3156,.T.);
#4202=ORIENTED_EDGE('',*,*,#3157,.T.);
#4203=ORIENTED_EDGE('',*,*,#3158,.T.);
#4204=ORIENTED_EDGE('',*,*,#3159,.T.);
#4205=ORIENTED_EDGE('',*,*,#3154,.F.);
#4206=ORIENTED_EDGE('',*,*,#3160,.T.);
#4207=ORIENTED_EDGE('',*,*,#3161,.T.);
#4208=ORIENTED_EDGE('',*,*,#3162,.T.);
#4209=ORIENTED_EDGE('',*,*,#3158,.F.);
#4210=ORIENTED_EDGE('',*,*,#3163,.T.);
#4211=ORIENTED_EDGE('',*,*,#3164,.T.);
#4212=ORIENTED_EDGE('',*,*,#3165,.T.);
#4213=ORIENTED_EDGE('',*,*,#3161,.F.);
#4214=ORIENTED_EDGE('',*,*,#3166,.T.);
#4215=ORIENTED_EDGE('',*,*,#3167,.T.);
#4216=ORIENTED_EDGE('',*,*,#3168,.T.);
#4217=ORIENTED_EDGE('',*,*,#3164,.F.);
#4218=ORIENTED_EDGE('',*,*,#3169,.T.);
#4219=ORIENTED_EDGE('',*,*,#3167,.F.);
#4220=ORIENTED_EDGE('',*,*,#3170,.T.);
#4221=ORIENTED_EDGE('',*,*,#3171,.T.);
#4222=ORIENTED_EDGE('',*,*,#3172,.T.);
#4223=ORIENTED_EDGE('',*,*,#3171,.F.);
#4224=ORIENTED_EDGE('',*,*,#3173,.T.);
#4225=ORIENTED_EDGE('',*,*,#3174,.T.);
#4226=ORIENTED_EDGE('',*,*,#3175,.T.);
#4227=ORIENTED_EDGE('',*,*,#3174,.F.);
#4228=ORIENTED_EDGE('',*,*,#3176,.T.);
#4229=ORIENTED_EDGE('',*,*,#3177,.T.);
#4230=ORIENTED_EDGE('',*,*,#3178,.T.);
#4231=ORIENTED_EDGE('',*,*,#3177,.F.);
#4232=ORIENTED_EDGE('',*,*,#3179,.T.);
#4233=ORIENTED_EDGE('',*,*,#3180,.T.);
#4234=ORIENTED_EDGE('',*,*,#3181,.T.);
#4235=ORIENTED_EDGE('',*,*,#3180,.F.);
#4236=ORIENTED_EDGE('',*,*,#3182,.T.);
#4237=ORIENTED_EDGE('',*,*,#3150,.F.);
#4238=ORIENTED_EDGE('',*,*,#3183,.T.);
#4239=ORIENTED_EDGE('',*,*,#3152,.F.);
#4240=ORIENTED_EDGE('',*,*,#3184,.T.);
#4241=ORIENTED_EDGE('',*,*,#3156,.F.);
#4242=ORIENTED_EDGE('',*,*,#3175,.F.);
#4243=ORIENTED_EDGE('',*,*,#3185,.T.);
#4244=ORIENTED_EDGE('',*,*,#3186,.F.);
#4245=ORIENTED_EDGE('',*,*,#3187,.T.);
#4246=ORIENTED_EDGE('',*,*,#3178,.F.);
#4247=ORIENTED_EDGE('',*,*,#3188,.F.);
#4248=ORIENTED_EDGE('',*,*,#3189,.F.);
#4249=ORIENTED_EDGE('',*,*,#3185,.F.);
#4250=ORIENTED_EDGE('',*,*,#3181,.F.);
#4251=ORIENTED_EDGE('',*,*,#3190,.T.);
#4252=ORIENTED_EDGE('',*,*,#3191,.F.);
#4253=ORIENTED_EDGE('',*,*,#3188,.T.);
#4254=ORIENTED_EDGE('',*,*,#3149,.F.);
#4255=ORIENTED_EDGE('',*,*,#3192,.F.);
#4256=ORIENTED_EDGE('',*,*,#3193,.F.);
#4257=ORIENTED_EDGE('',*,*,#3190,.F.);
#4258=ORIENTED_EDGE('',*,*,#3183,.F.);
#4259=ORIENTED_EDGE('',*,*,#3194,.T.);
#4260=ORIENTED_EDGE('',*,*,#3195,.F.);
#4261=ORIENTED_EDGE('',*,*,#3192,.T.);
#4262=ORIENTED_EDGE('',*,*,#3155,.F.);
#4263=ORIENTED_EDGE('',*,*,#3196,.F.);
#4264=ORIENTED_EDGE('',*,*,#3197,.F.);
#4265=ORIENTED_EDGE('',*,*,#3194,.F.);
#4266=ORIENTED_EDGE('',*,*,#3153,.F.);
#4267=ORIENTED_EDGE('',*,*,#3184,.F.);
#4268=ORIENTED_EDGE('',*,*,#3151,.F.);
#4269=ORIENTED_EDGE('',*,*,#3182,.F.);
#4270=ORIENTED_EDGE('',*,*,#3179,.F.);
#4271=ORIENTED_EDGE('',*,*,#3176,.F.);
#4272=ORIENTED_EDGE('',*,*,#3173,.F.);
#4273=ORIENTED_EDGE('',*,*,#3170,.F.);
#4274=ORIENTED_EDGE('',*,*,#3166,.F.);
#4275=ORIENTED_EDGE('',*,*,#3163,.F.);
#4276=ORIENTED_EDGE('',*,*,#3160,.F.);
#4277=ORIENTED_EDGE('',*,*,#3157,.F.);
#4278=ORIENTED_EDGE('',*,*,#3198,.T.);
#4279=ORIENTED_EDGE('',*,*,#3199,.T.);
#4280=ORIENTED_EDGE('',*,*,#3193,.T.);
#4281=ORIENTED_EDGE('',*,*,#3200,.F.);
#4282=ORIENTED_EDGE('',*,*,#3201,.T.);
#4283=ORIENTED_EDGE('',*,*,#3202,.T.);
#4284=ORIENTED_EDGE('',*,*,#3191,.T.);
#4285=ORIENTED_EDGE('',*,*,#3199,.F.);
#4286=ORIENTED_EDGE('',*,*,#3203,.T.);
#4287=ORIENTED_EDGE('',*,*,#3204,.T.);
#4288=ORIENTED_EDGE('',*,*,#3189,.T.);
#4289=ORIENTED_EDGE('',*,*,#3202,.F.);
#4290=ORIENTED_EDGE('',*,*,#3205,.T.);
#4291=ORIENTED_EDGE('',*,*,#3206,.T.);
#4292=ORIENTED_EDGE('',*,*,#3186,.T.);
#4293=ORIENTED_EDGE('',*,*,#3204,.F.);
#4294=ORIENTED_EDGE('',*,*,#3207,.T.);
#4295=ORIENTED_EDGE('',*,*,#3208,.T.);
#4296=ORIENTED_EDGE('',*,*,#3209,.T.);
#4297=ORIENTED_EDGE('',*,*,#3206,.F.);
#4298=ORIENTED_EDGE('',*,*,#3210,.T.);
#4299=ORIENTED_EDGE('',*,*,#3208,.F.);
#4300=ORIENTED_EDGE('',*,*,#3211,.T.);
#4301=ORIENTED_EDGE('',*,*,#3212,.T.);
#4302=ORIENTED_EDGE('',*,*,#3213,.T.);
#4303=ORIENTED_EDGE('',*,*,#3212,.F.);
#4304=ORIENTED_EDGE('',*,*,#3214,.T.);
#4305=ORIENTED_EDGE('',*,*,#3215,.T.);
#4306=ORIENTED_EDGE('',*,*,#3216,.T.);
#4307=ORIENTED_EDGE('',*,*,#3215,.F.);
#4308=ORIENTED_EDGE('',*,*,#3217,.T.);
#4309=ORIENTED_EDGE('',*,*,#3218,.T.);
#4310=ORIENTED_EDGE('',*,*,#3219,.T.);
#4311=ORIENTED_EDGE('',*,*,#3218,.F.);
#4312=ORIENTED_EDGE('',*,*,#3220,.T.);
#4313=ORIENTED_EDGE('',*,*,#3221,.T.);
#4314=ORIENTED_EDGE('',*,*,#3222,.T.);
#4315=ORIENTED_EDGE('',*,*,#3221,.F.);
#4316=ORIENTED_EDGE('',*,*,#3223,.T.);
#4317=ORIENTED_EDGE('',*,*,#3224,.T.);
#4318=ORIENTED_EDGE('',*,*,#3197,.T.);
#4319=ORIENTED_EDGE('',*,*,#3224,.F.);
#4320=ORIENTED_EDGE('',*,*,#3225,.T.);
#4321=ORIENTED_EDGE('',*,*,#3226,.T.);
#4322=ORIENTED_EDGE('',*,*,#3195,.T.);
#4323=ORIENTED_EDGE('',*,*,#3226,.F.);
#4324=ORIENTED_EDGE('',*,*,#3227,.T.);
#4325=ORIENTED_EDGE('',*,*,#3200,.T.);
#4326=ORIENTED_EDGE('',*,*,#3165,.F.);
#4327=ORIENTED_EDGE('',*,*,#3228,.T.);
#4328=ORIENTED_EDGE('',*,*,#3216,.F.);
#4329=ORIENTED_EDGE('',*,*,#3229,.T.);
#4330=ORIENTED_EDGE('',*,*,#3162,.F.);
#4331=ORIENTED_EDGE('',*,*,#3229,.F.);
#4332=ORIENTED_EDGE('',*,*,#3219,.F.);
#4333=ORIENTED_EDGE('',*,*,#3230,.F.);
#4334=ORIENTED_EDGE('',*,*,#3159,.F.);
#4335=ORIENTED_EDGE('',*,*,#3230,.T.);
#4336=ORIENTED_EDGE('',*,*,#3222,.F.);
#4337=ORIENTED_EDGE('',*,*,#3196,.T.);
#4338=ORIENTED_EDGE('',*,*,#3198,.F.);
#4339=ORIENTED_EDGE('',*,*,#3227,.F.);
#4340=ORIENTED_EDGE('',*,*,#3225,.F.);
#4341=ORIENTED_EDGE('',*,*,#3223,.F.);
#4342=ORIENTED_EDGE('',*,*,#3220,.F.);
#4343=ORIENTED_EDGE('',*,*,#3217,.F.);
#4344=ORIENTED_EDGE('',*,*,#3214,.F.);
#4345=ORIENTED_EDGE('',*,*,#3211,.F.);
#4346=ORIENTED_EDGE('',*,*,#3207,.F.);
#4347=ORIENTED_EDGE('',*,*,#3205,.F.);
#4348=ORIENTED_EDGE('',*,*,#3203,.F.);
#4349=ORIENTED_EDGE('',*,*,#3201,.F.);
#4350=ORIENTED_EDGE('',*,*,#3169,.F.);
#4351=ORIENTED_EDGE('',*,*,#3231,.T.);
#4352=ORIENTED_EDGE('',*,*,#3210,.F.);
#4353=ORIENTED_EDGE('',*,*,#3232,.T.);
#4354=ORIENTED_EDGE('',*,*,#3168,.F.);
#4355=ORIENTED_EDGE('',*,*,#3232,.F.);
#4356=ORIENTED_EDGE('',*,*,#3213,.F.);
#4357=ORIENTED_EDGE('',*,*,#3228,.F.);
#4358=ORIENTED_EDGE('',*,*,#3172,.F.);
#4359=ORIENTED_EDGE('',*,*,#3187,.F.);
#4360=ORIENTED_EDGE('',*,*,#3209,.F.);
#4361=ORIENTED_EDGE('',*,*,#3231,.F.);
#5373=CYLINDRICAL_SURFACE('',#6174,1.);
#5374=CYLINDRICAL_SURFACE('',#6177,1.);
#5375=CYLINDRICAL_SURFACE('',#6180,1.);
#5376=CYLINDRICAL_SURFACE('',#6182,1.);
#5377=CYLINDRICAL_SURFACE('',#6184,1.);
#5378=CYLINDRICAL_SURFACE('',#6186,1.);
#5379=CYLINDRICAL_SURFACE('',#6188,1.);
#5380=CYLINDRICAL_SURFACE('',#6190,1.);
#5381=CYLINDRICAL_SURFACE('',#6192,1.);
#5382=CYLINDRICAL_SURFACE('',#6194,1.);
#5383=CYLINDRICAL_SURFACE('',#6196,1.);
#5384=CYLINDRICAL_SURFACE('',#6197,1.);
#5385=CYLINDRICAL_SURFACE('',#6205,1.);
#5386=CYLINDRICAL_SURFACE('',#6208,1.);
#5387=CYLINDRICAL_SURFACE('',#6210,1.);
#5388=CYLINDRICAL_SURFACE('',#6212,1.);
#5389=CYLINDRICAL_SURFACE('',#6214,1.);
#5390=CYLINDRICAL_SURFACE('',#6216,1.);
#5391=CYLINDRICAL_SURFACE('',#6218,1.);
#5392=CYLINDRICAL_SURFACE('',#6220,1.);
#5393=CYLINDRICAL_SURFACE('',#6222,1.);
#5394=CYLINDRICAL_SURFACE('',#6224,1.);
#5395=CYLINDRICAL_SURFACE('',#6226,1.);
#5396=CYLINDRICAL_SURFACE('',#6228,1.);
#5629=ADVANCED_FACE('',(#566),#5373,.T.);
#5630=ADVANCED_FACE('',(#567),#5374,.T.);
#5631=ADVANCED_FACE('',(#568),#5375,.T.);
#5632=ADVANCED_FACE('',(#569),#5376,.T.);
#5633=ADVANCED_FACE('',(#570),#5377,.T.);
#5634=ADVANCED_FACE('',(#571),#5378,.T.);
#5635=ADVANCED_FACE('',(#572),#5379,.T.);
#5636=ADVANCED_FACE('',(#573),#5380,.T.);
#5637=ADVANCED_FACE('',(#574),#5381,.T.);
#5638=ADVANCED_FACE('',(#575),#5382,.T.);
#5639=ADVANCED_FACE('',(#576),#5383,.T.);
#5640=ADVANCED_FACE('',(#577),#5384,.T.);
#5641=ADVANCED_FACE('',(#578),#374,.T.);
#5642=ADVANCED_FACE('',(#579),#375,.T.);
#5643=ADVANCED_FACE('',(#580),#376,.T.);
#5644=ADVANCED_FACE('',(#581),#377,.T.);
#5645=ADVANCED_FACE('',(#582),#378,.T.);
#5646=ADVANCED_FACE('',(#583),#379,.T.);
#5647=ADVANCED_FACE('',(#584),#380,.F.);
#5648=ADVANCED_FACE('',(#585),#5385,.T.);
#5649=ADVANCED_FACE('',(#586),#5386,.T.);
#5650=ADVANCED_FACE('',(#587),#5387,.T.);
#5651=ADVANCED_FACE('',(#588),#5388,.T.);
#5652=ADVANCED_FACE('',(#589),#5389,.T.);
#5653=ADVANCED_FACE('',(#590),#5390,.T.);
#5654=ADVANCED_FACE('',(#591),#5391,.T.);
#5655=ADVANCED_FACE('',(#592),#5392,.T.);
#5656=ADVANCED_FACE('',(#593),#5393,.T.);
#5657=ADVANCED_FACE('',(#594),#5394,.T.);
#5658=ADVANCED_FACE('',(#595),#5395,.T.);
#5659=ADVANCED_FACE('',(#596),#5396,.T.);
#5660=ADVANCED_FACE('',(#597),#381,.T.);
#5661=ADVANCED_FACE('',(#598),#382,.T.);
#5662=ADVANCED_FACE('',(#599),#383,.T.);
#5663=ADVANCED_FACE('',(#600),#384,.T.);
#5664=ADVANCED_FACE('',(#601),#385,.T.);
#5665=ADVANCED_FACE('',(#602),#386,.T.);
#5666=ADVANCED_FACE('',(#603),#387,.T.);
#5882=CLOSED_SHELL('',(#5629,#5630,#5631,#5632,#5633,#5634,#5635,#5636,
#5637,#5638,#5639,#5640,#5641,#5642,#5643,#5644,#5645,#5646,#5647,#5648,
#5649,#5650,#5651,#5652,#5653,#5654,#5655,#5656,#5657,#5658,#5659,#5660,
#5661,#5662,#5663,#5664,#5665,#5666));
#6173=AXIS2_PLACEMENT_3D('',#8940,#7133,#7134);
#6174=AXIS2_PLACEMENT_3D('',#8941,#7135,#7136);
#6175=AXIS2_PLACEMENT_3D('',#8946,#7138,#7139);
#6176=AXIS2_PLACEMENT_3D('',#8949,#7141,#7142);
#6177=AXIS2_PLACEMENT_3D('',#8950,#7143,#7144);
#6178=AXIS2_PLACEMENT_3D('',#8955,#7146,#7147);
#6179=AXIS2_PLACEMENT_3D('',#8958,#7149,#7150);
#6180=AXIS2_PLACEMENT_3D('',#8959,#7151,#7152);
#6181=AXIS2_PLACEMENT_3D('',#8963,#7154,#7155);
#6182=AXIS2_PLACEMENT_3D('',#8965,#7157,#7158);
#6183=AXIS2_PLACEMENT_3D('',#8969,#7160,#7161);
#6184=AXIS2_PLACEMENT_3D('',#8971,#7163,#7164);
#6185=AXIS2_PLACEMENT_3D('',#8975,#7166,#7167);
#6186=AXIS2_PLACEMENT_3D('',#8977,#7169,#7170);
#6187=AXIS2_PLACEMENT_3D('',#8981,#7172,#7173);
#6188=AXIS2_PLACEMENT_3D('',#8983,#7175,#7176);
#6189=AXIS2_PLACEMENT_3D('',#8988,#7179,#7180);
#6190=AXIS2_PLACEMENT_3D('',#8989,#7181,#7182);
#6191=AXIS2_PLACEMENT_3D('',#8994,#7185,#7186);
#6192=AXIS2_PLACEMENT_3D('',#8995,#7187,#7188);
#6193=AXIS2_PLACEMENT_3D('',#9000,#7191,#7192);
#6194=AXIS2_PLACEMENT_3D('',#9001,#7193,#7194);
#6195=AXIS2_PLACEMENT_3D('',#9006,#7197,#7198);
#6196=AXIS2_PLACEMENT_3D('',#9007,#7199,#7200);
#6197=AXIS2_PLACEMENT_3D('',#9010,#7203,#7204);
#6198=AXIS2_PLACEMENT_3D('',#9013,#7207,#7208);
#6199=AXIS2_PLACEMENT_3D('',#9019,#7212,#7213);
#6200=AXIS2_PLACEMENT_3D('',#9023,#7216,#7217);
#6201=AXIS2_PLACEMENT_3D('',#9027,#7220,#7221);
#6202=AXIS2_PLACEMENT_3D('',#9031,#7224,#7225);
#6203=AXIS2_PLACEMENT_3D('',#9035,#7228,#7229);
#6204=AXIS2_PLACEMENT_3D('',#9039,#7232,#7233);
#6205=AXIS2_PLACEMENT_3D('',#9040,#7234,#7235);
#6206=AXIS2_PLACEMENT_3D('',#9044,#7237,#7238);
#6207=AXIS2_PLACEMENT_3D('',#9045,#7239,#7240);
#6208=AXIS2_PLACEMENT_3D('',#9046,#7241,#7242);
#6209=AXIS2_PLACEMENT_3D('',#9049,#7244,#7245);
#6210=AXIS2_PLACEMENT_3D('',#9050,#7246,#7247);
#6211=AXIS2_PLACEMENT_3D('',#9053,#7249,#7250);
#6212=AXIS2_PLACEMENT_3D('',#9054,#7251,#7252);
#6213=AXIS2_PLACEMENT_3D('',#9057,#7254,#7255);
#6214=AXIS2_PLACEMENT_3D('',#9058,#7256,#7257);
#6215=AXIS2_PLACEMENT_3D('',#9062,#7259,#7260);
#6216=AXIS2_PLACEMENT_3D('',#9064,#7262,#7263);
#6217=AXIS2_PLACEMENT_3D('',#9069,#7266,#7267);
#6218=AXIS2_PLACEMENT_3D('',#9070,#7268,#7269);
#6219=AXIS2_PLACEMENT_3D('',#9075,#7272,#7273);
#6220=AXIS2_PLACEMENT_3D('',#9076,#7274,#7275);
#6221=AXIS2_PLACEMENT_3D('',#9081,#7278,#7279);
#6222=AXIS2_PLACEMENT_3D('',#9082,#7280,#7281);
#6223=AXIS2_PLACEMENT_3D('',#9087,#7284,#7285);
#6224=AXIS2_PLACEMENT_3D('',#9088,#7286,#7287);
#6225=AXIS2_PLACEMENT_3D('',#9092,#7290,#7291);
#6226=AXIS2_PLACEMENT_3D('',#9093,#7292,#7293);
#6227=AXIS2_PLACEMENT_3D('',#9096,#7295,#7296);
#6228=AXIS2_PLACEMENT_3D('',#9097,#7297,#7298);
#6229=AXIS2_PLACEMENT_3D('',#9099,#7300,#7301);
#6230=AXIS2_PLACEMENT_3D('',#9102,#7304,#7305);
#6231=AXIS2_PLACEMENT_3D('',#9104,#7307,#7308);
#6232=AXIS2_PLACEMENT_3D('',#9105,#7309,#7310);
#6233=AXIS2_PLACEMENT_3D('',#9106,#7311,#7312);
#6234=AXIS2_PLACEMENT_3D('',#9109,#7315,#7316);
#6235=AXIS2_PLACEMENT_3D('',#9110,#7317,#7318);
#7133=DIRECTION('axis',(0.,0.,1.));
#7134=DIRECTION('refdir',(1.,0.,0.));
#7135=DIRECTION('center_axis',(0.,1.,0.));
#7136=DIRECTION('ref_axis',(0.707106781186548,0.,-0.707106781186548));
#7137=DIRECTION('',(0.,-1.,0.));
#7138=DIRECTION('center_axis',(0.38268343236509,0.923879532511287,0.));
#7139=DIRECTION('ref_axis',(0.923879532511287,-0.38268343236509,0.));
#7140=DIRECTION('',(0.,1.,0.));
#7141=DIRECTION('center_axis',(-0.382683432365087,-0.923879532511288,0.));
#7142=DIRECTION('ref_axis',(0.923879532511288,-0.382683432365087,0.));
#7143=DIRECTION('center_axis',(1.,0.,0.));
#7144=DIRECTION('ref_axis',(0.,-0.707106781186548,-0.707106781186548));
#7145=DIRECTION('',(1.,0.,0.));
#7146=DIRECTION('center_axis',(-0.923879532511287,-0.38268343236509,0.));
#7147=DIRECTION('ref_axis',(-0.38268343236509,0.923879532511287,0.));
#7148=DIRECTION('',(-1.,0.,0.));
#7149=DIRECTION('center_axis',(0.923879532511288,0.382683432365087,-5.80230514691304E-15));
#7150=DIRECTION('ref_axis',(-0.382683432365087,0.923879532511288,-1.40080037787048E-14));
#7151=DIRECTION('center_axis',(0.707106781186548,0.707106781186548,0.));
#7152=DIRECTION('ref_axis',(0.499999999999998,-0.499999999999998,-0.70710678118655));
#7153=DIRECTION('',(0.707106781186548,0.707106781186548,0.));
#7154=DIRECTION('center_axis',(-0.382683432365095,-0.923879532511285,0.));
#7155=DIRECTION('ref_axis',(-0.923879532511285,0.382683432365095,0.));
#7156=DIRECTION('',(-0.707106781186548,-0.707106781186548,0.));
#7157=DIRECTION('center_axis',(0.,-1.,0.));
#7158=DIRECTION('ref_axis',(0.707106781186548,0.,-0.707106781186548));
#7159=DIRECTION('',(0.,1.,0.));
#7160=DIRECTION('center_axis',(0.382683432365099,-0.923879532511283,-8.20569863179165E-15));
#7161=DIRECTION('ref_axis',(0.923879532511283,0.382683432365098,-1.98103089256172E-14));
#7162=DIRECTION('',(0.,-1.,0.));
#7163=DIRECTION('center_axis',(-0.707106781186548,0.707106781186548,0.));
#7164=DIRECTION('ref_axis',(0.499999999999998,0.499999999999998,-0.70710678118655));
#7165=DIRECTION('',(-0.707106781186548,0.707106781186548,0.));
#7166=DIRECTION('center_axis',(0.923879532511286,-0.382683432365092,0.));
#7167=DIRECTION('ref_axis',(-0.382683432365092,-0.923879532511286,0.));
#7168=DIRECTION('',(0.707106781186548,-0.707106781186548,0.));
#7169=DIRECTION('center_axis',(1.,0.,0.));
#7170=DIRECTION('ref_axis',(0.,0.707106781186548,-0.707106781186548));
#7171=DIRECTION('',(-1.,0.,0.));
#7172=DIRECTION('center_axis',(0.923879532511286,0.382683432365092,0.));
#7173=DIRECTION('ref_axis',(-0.382683432365092,0.923879532511286,0.));
#7174=DIRECTION('',(1.,0.,0.));
#7175=DIRECTION('center_axis',(-0.707106781186548,-0.707106781186548,0.));
#7176=DIRECTION('ref_axis',(-0.499999999999998,0.499999999999998,-0.70710678118655));
#7177=DIRECTION('',(0.707106781186548,0.707106781186548,0.));
#7178=DIRECTION('',(-0.707106781186548,-0.707106781186548,0.));
#7179=DIRECTION('center_axis',(0.382683432365092,0.923879532511286,0.));
#7180=DIRECTION('ref_axis',(0.923879532511286,-0.382683432365092,0.));
#7181=DIRECTION('center_axis',(0.,1.,0.));
#7182=DIRECTION('ref_axis',(-0.707106781186548,0.,-0.707106781186548));
#7183=DIRECTION('',(0.,1.,0.));
#7184=DIRECTION('',(0.,-1.,0.));
#7185=DIRECTION('center_axis',(-0.382683432365092,0.923879532511286,0.));
#7186=DIRECTION('ref_axis',(-0.923879532511286,-0.382683432365092,0.));
#7187=DIRECTION('center_axis',(0.707106781186548,-0.707106781186548,0.));
#7188=DIRECTION('ref_axis',(-0.499999999999998,-0.499999999999998,-0.70710678118655));
#7189=DIRECTION('',(-0.707106781186548,0.707106781186548,0.));
#7190=DIRECTION('',(0.707106781186548,-0.707106781186548,0.));
#7191=DIRECTION('center_axis',(-0.923879532511286,0.382683432365092,0.));
#7192=DIRECTION('ref_axis',(0.382683432365092,0.923879532511286,0.));
#7193=DIRECTION('center_axis',(-1.,0.,0.));
#7194=DIRECTION('ref_axis',(0.,-0.707106781186548,-0.707106781186548));
#7195=DIRECTION('',(-1.,0.,0.));
#7196=DIRECTION('',(1.,0.,0.));
#7197=DIRECTION('center_axis',(-0.923879532511286,-0.382683432365092,4.10284931589584E-15));
#7198=DIRECTION('ref_axis',(0.382683432365092,-0.923879532511286,9.90515446280885E-15));
#7199=DIRECTION('center_axis',(0.707106781186548,0.707106781186548,0.));
#7200=DIRECTION('ref_axis',(0.499999999999998,-0.499999999999998,-0.70710678118655));
#7201=DIRECTION('',(-0.707106781186548,-0.707106781186548,0.));
#7202=DIRECTION('',(0.707106781186548,0.707106781186548,0.));
#7203=DIRECTION('center_axis',(0.707106781186548,0.707106781186548,0.));
#7204=DIRECTION('ref_axis',(0.499999999999998,-0.499999999999998,-0.70710678118655));
#7205=DIRECTION('',(-0.707106781186548,-0.707106781186548,0.));
#7206=DIRECTION('',(0.707106781186548,0.707106781186548,0.));
#7207=DIRECTION('center_axis',(-0.707106781186548,-0.707106781186548,0.));
#7208=DIRECTION('ref_axis',(0.,0.,1.));
#7209=DIRECTION('',(0.,0.,1.));
#7210=DIRECTION('',(0.707106781186548,-0.707106781186548,0.));
#7211=DIRECTION('',(0.,0.,-1.));
#7212=DIRECTION('center_axis',(0.,-1.,0.));
#7213=DIRECTION('ref_axis',(1.,0.,0.));
#7214=DIRECTION('',(0.,0.,-1.));
#7215=DIRECTION('',(1.,0.,0.));
#7216=DIRECTION('center_axis',(0.707106781186548,-0.707106781186548,0.));
#7217=DIRECTION('ref_axis',(0.,0.,-1.));
#7218=DIRECTION('',(0.,0.,1.));
#7219=DIRECTION('',(0.707106781186548,0.707106781186548,0.));
#7220=DIRECTION('center_axis',(1.,0.,0.));
#7221=DIRECTION('ref_axis',(0.,1.,0.));
#7222=DIRECTION('',(0.,0.,-1.));
#7223=DIRECTION('',(0.,1.,0.));
#7224=DIRECTION('center_axis',(0.707106781186548,-0.707106781186548,0.));
#7225=DIRECTION('ref_axis',(0.,0.,-1.));
#7226=DIRECTION('',(0.,0.,1.));
#7227=DIRECTION('',(0.707106781186548,0.707106781186548,0.));
#7228=DIRECTION('center_axis',(0.,-1.,0.));
#7229=DIRECTION('ref_axis',(1.,0.,0.));
#7230=DIRECTION('',(0.,0.,-1.));
#7231=DIRECTION('',(1.,0.,0.));
#7232=DIRECTION('center_axis',(0.,0.,1.));
#7233=DIRECTION('ref_axis',(-1.,0.,0.));
#7234=DIRECTION('center_axis',(0.,1.,0.));
#7235=DIRECTION('ref_axis',(0.707106781186551,0.,0.707106781186544));
#7236=DIRECTION('',(0.,-1.,0.));
#7237=DIRECTION('center_axis',(0.38268343236509,0.923879532511287,0.));
#7238=DIRECTION('ref_axis',(0.923879532511287,-0.38268343236509,0.));
#7239=DIRECTION('center_axis',(0.382683432365087,0.923879532511288,0.));
#7240=DIRECTION('ref_axis',(0.923879532511288,-0.382683432365087,0.));
#7241=DIRECTION('center_axis',(-0.707106781186548,-0.707106781186548,0.));
#7242=DIRECTION('ref_axis',(0.499999999999998,-0.499999999999998,0.70710678118655));
#7243=DIRECTION('',(-0.707106781186548,-0.707106781186548,0.));
#7244=DIRECTION('center_axis',(0.923879532511285,0.382683432365095,-4.10284931589581E-15));
#7245=DIRECTION('ref_axis',(-0.382683432365095,0.923879532511285,9.905154462809E-15));
#7246=DIRECTION('center_axis',(1.,0.,0.));
#7247=DIRECTION('ref_axis',(0.,-0.707106781186548,0.707106781186548));
#7248=DIRECTION('',(-1.,0.,0.));
#7249=DIRECTION('center_axis',(0.923879532511286,-0.382683432365092,0.));
#7250=DIRECTION('ref_axis',(-0.382683432365092,-0.923879532511286,0.));
#7251=DIRECTION('center_axis',(-0.707106781186548,0.707106781186548,0.));
#7252=DIRECTION('ref_axis',(-0.499999999999998,-0.499999999999998,0.70710678118655));
#7253=DIRECTION('',(-0.707106781186548,0.707106781186548,0.));
#7254=DIRECTION('center_axis',(0.382683432365092,-0.923879532511286,0.));
#7255=DIRECTION('ref_axis',(0.923879532511286,0.382683432365092,0.));
#7256=DIRECTION('center_axis',(0.,-1.,0.));
#7257=DIRECTION('ref_axis',(-0.707106781186548,0.,0.707106781186548));
#7258=DIRECTION('',(0.,1.,0.));
#7259=DIRECTION('center_axis',(-0.382683432365092,-0.923879532511286,0.));
#7260=DIRECTION('ref_axis',(-0.923879532511286,0.382683432365092,0.));
#7261=DIRECTION('',(0.,-1.,0.));
#7262=DIRECTION('center_axis',(0.707106781186548,0.707106781186548,0.));
#7263=DIRECTION('ref_axis',(-0.499999999999998,0.499999999999998,0.70710678118655));
#7264=DIRECTION('',(-0.707106781186548,-0.707106781186548,0.));
#7265=DIRECTION('',(0.707106781186548,0.707106781186548,0.));
#7266=DIRECTION('center_axis',(-0.923879532511286,-0.382683432365092,0.));
#7267=DIRECTION('ref_axis',(0.382683432365092,-0.923879532511286,0.));
#7268=DIRECTION('center_axis',(-1.,0.,0.));
#7269=DIRECTION('ref_axis',(0.,0.707106781186548,0.707106781186548));
#7270=DIRECTION('',(-1.,0.,0.));
#7271=DIRECTION('',(1.,0.,0.));
#7272=DIRECTION('center_axis',(-0.923879532511286,0.382683432365092,0.));
#7273=DIRECTION('ref_axis',(0.382683432365092,0.923879532511286,0.));
#7274=DIRECTION('center_axis',(0.707106781186548,-0.707106781186548,0.));
#7275=DIRECTION('ref_axis',(0.499999999999998,0.499999999999998,0.70710678118655));
#7276=DIRECTION('',(-0.707106781186548,0.707106781186548,0.));
#7277=DIRECTION('',(0.707106781186548,-0.707106781186548,0.));
#7278=DIRECTION('center_axis',(-0.382683432365092,0.923879532511286,0.));
#7279=DIRECTION('ref_axis',(-0.923879532511286,-0.382683432365092,0.));
#7280=DIRECTION('center_axis',(0.,1.,0.));
#7281=DIRECTION('ref_axis',(0.707106781186548,0.,0.707106781186548));
#7282=DIRECTION('',(0.,1.,0.));
#7283=DIRECTION('',(0.,-1.,0.));
#7284=DIRECTION('center_axis',(0.382683432365092,0.923879532511286,-4.10284931589584E-15));
#7285=DIRECTION('ref_axis',(0.923879532511286,-0.382683432365092,-9.90515446280885E-15));
#7286=DIRECTION('center_axis',(-0.707106781186548,-0.707106781186548,0.));
#7287=DIRECTION('ref_axis',(0.499999999999998,-0.499999999999998,0.70710678118655));
#7288=DIRECTION('',(0.707106781186548,0.707106781186548,0.));
#7289=DIRECTION('',(-0.707106781186548,-0.707106781186548,0.));
#7290=DIRECTION('center_axis',(0.923879532511287,0.38268343236509,0.));
#7291=DIRECTION('ref_axis',(-0.38268343236509,0.923879532511287,0.));
#7292=DIRECTION('center_axis',(1.,0.,0.));
#7293=DIRECTION('ref_axis',(0.,-0.707106781186551,0.707106781186544));
#7294=DIRECTION('',(-1.,0.,0.));
#7295=DIRECTION('center_axis',(0.923879532511288,0.382683432365087,5.80230514691306E-15));
#7296=DIRECTION('ref_axis',(-0.382683432365087,0.923879532511288,1.40080037787049E-14));
#7297=DIRECTION('center_axis',(-0.707106781186548,-0.707106781186548,0.));
#7298=DIRECTION('ref_axis',(0.499999999999998,-0.499999999999998,0.70710678118655));
#7299=DIRECTION('',(-0.707106781186548,-0.707106781186548,0.));
#7300=DIRECTION('center_axis',(0.707106781186548,0.707106781186548,0.));
#7301=DIRECTION('ref_axis',(0.,0.,-1.));
#7302=DIRECTION('',(0.,0.,1.));
#7303=DIRECTION('',(0.,0.,-1.));
#7304=DIRECTION('center_axis',(1.,0.,0.));
#7305=DIRECTION('ref_axis',(0.,1.,0.));
#7306=DIRECTION('',(0.,0.,1.));
#7307=DIRECTION('center_axis',(0.707106781186548,-0.707106781186548,0.));
#7308=DIRECTION('ref_axis',(0.,0.,-1.));
#7309=DIRECTION('center_axis',(0.,0.,1.));
#7310=DIRECTION('ref_axis',(1.,0.,0.));
#7311=DIRECTION('center_axis',(-0.707106781186548,0.707106781186548,0.));
#7312=DIRECTION('ref_axis',(0.,0.,1.));
#7313=DIRECTION('',(0.,0.,1.));
#7314=DIRECTION('',(0.,0.,-1.));
#7315=DIRECTION('center_axis',(0.,1.,0.));
#7316=DIRECTION('ref_axis',(-1.,0.,0.));
#7317=DIRECTION('center_axis',(-1.,0.,0.));
#7318=DIRECTION('ref_axis',(0.,-1.,0.));
#8940=CARTESIAN_POINT('',(0.,0.,0.));
#8941=CARTESIAN_POINT('Origin',(29.,-25.,21.));
#8942=CARTESIAN_POINT('',(30.,-35.,21.));
#8943=CARTESIAN_POINT('',(30.,-45.,21.));
#8944=CARTESIAN_POINT('',(30.,-25.,21.));
#8945=CARTESIAN_POINT('',(29.,-44.5857864376269,20.));
#8946=CARTESIAN_POINT('Origin',(29.,-44.5857864376269,21.));
#8947=CARTESIAN_POINT('',(29.,-34.5857864376269,20.));
#8948=CARTESIAN_POINT('',(29.,-25.,20.));
#8949=CARTESIAN_POINT('Origin',(29.,-34.5857864376269,21.));
#8950=CARTESIAN_POINT('Origin',(15.,-29.,21.));
#8951=CARTESIAN_POINT('',(34.5857864376269,-29.,20.));
#8952=CARTESIAN_POINT('',(44.5857864376269,-29.,20.));
#8953=CARTESIAN_POINT('',(15.,-29.,20.));
#8954=CARTESIAN_POINT('',(45.,-30.,21.));
#8955=CARTESIAN_POINT('Origin',(44.5857864376269,-29.,21.));
#8956=CARTESIAN_POINT('',(35.,-30.,21.));
#8957=CARTESIAN_POINT('',(15.,-30.,21.));
#8958=CARTESIAN_POINT('Origin',(34.5857864376269,-29.,21.));
#8959=CARTESIAN_POINT('Origin',(41.7928932188135,-31.7928932188135,21.));
#8960=CARTESIAN_POINT('',(49.,-24.5857864376269,20.));
#8961=CARTESIAN_POINT('',(41.7928932188135,-31.7928932188135,20.));
#8962=CARTESIAN_POINT('',(50.,-25.,21.));
#8963=CARTESIAN_POINT('Origin',(49.,-24.5857864376269,21.));
#8964=CARTESIAN_POINT('',(42.5,-32.5,21.));
#8965=CARTESIAN_POINT('Origin',(49.,-15.,21.));
#8966=CARTESIAN_POINT('',(49.,44.5857864376269,20.));
#8967=CARTESIAN_POINT('',(49.,-15.,20.));
#8968=CARTESIAN_POINT('',(50.,45.,21.));
#8969=CARTESIAN_POINT('Origin',(49.,44.5857864376269,21.));
#8970=CARTESIAN_POINT('',(50.,-15.,21.));
#8971=CARTESIAN_POINT('Origin',(46.7928932188135,46.7928932188135,21.));
#8972=CARTESIAN_POINT('',(44.5857864376269,49.,20.));
#8973=CARTESIAN_POINT('',(46.7928932188135,46.7928932188135,20.));
#8974=CARTESIAN_POINT('',(45.,50.,21.));
#8975=CARTESIAN_POINT('Origin',(44.5857864376269,49.,21.));
#8976=CARTESIAN_POINT('',(47.5,47.5,21.));
#8977=CARTESIAN_POINT('Origin',(25.,49.,21.));
#8978=CARTESIAN_POINT('',(-44.5857864376269,49.,20.));
#8979=CARTESIAN_POINT('',(25.,49.,20.));
#8980=CARTESIAN_POINT('',(-45.,50.,21.));
#8981=CARTESIAN_POINT('Origin',(-44.5857864376269,49.,21.));
#8982=CARTESIAN_POINT('',(25.,50.,21.));
#8983=CARTESIAN_POINT('Origin',(-46.7928932188135,46.7928932188135,21.));
#8984=CARTESIAN_POINT('',(-50.,45.,21.));
#8985=CARTESIAN_POINT('',(-47.5,47.5,21.));
#8986=CARTESIAN_POINT('',(-49.,44.5857864376269,20.));
#8987=CARTESIAN_POINT('',(-46.7928932188135,46.7928932188135,20.));
#8988=CARTESIAN_POINT('Origin',(-49.,44.5857864376269,21.));
#8989=CARTESIAN_POINT('Origin',(-49.,25.,21.));
#8990=CARTESIAN_POINT('',(-50.,-45.,21.));
#8991=CARTESIAN_POINT('',(-50.,25.,21.));
#8992=CARTESIAN_POINT('',(-49.,-44.5857864376269,20.));
#8993=CARTESIAN_POINT('',(-49.,25.,20.));
#8994=CARTESIAN_POINT('Origin',(-49.,-44.5857864376269,21.));
#8995=CARTESIAN_POINT('Origin',(-46.7928932188135,-46.7928932188135,21.));
#8996=CARTESIAN_POINT('',(-45.,-50.,21.));
#8997=CARTESIAN_POINT('',(-47.5,-47.5,21.));
#8998=CARTESIAN_POINT('',(-44.5857864376269,-49.,20.));
#8999=CARTESIAN_POINT('',(-46.7928932188135,-46.7928932188135,20.));
#9000=CARTESIAN_POINT('Origin',(-44.5857864376269,-49.,21.));
#9001=CARTESIAN_POINT('Origin',(-25.,-49.,21.));
#9002=CARTESIAN_POINT('',(25.,-50.,21.));
#9003=CARTESIAN_POINT('',(-25.,-50.,21.));
#9004=CARTESIAN_POINT('',(24.5857864376269,-49.,20.));
#9005=CARTESIAN_POINT('',(-25.,-49.,20.));
#9006=CARTESIAN_POINT('Origin',(24.5857864376269,-49.,21.));
#9007=CARTESIAN_POINT('Origin',(31.7928932188135,-41.7928932188135,21.));
#9008=CARTESIAN_POINT('',(32.5,-42.5,21.));
#9009=CARTESIAN_POINT('',(31.7928932188135,-41.7928932188135,20.));
#9010=CARTESIAN_POINT('Origin',(31.7928932188135,-31.7928932188135,21.));
#9011=CARTESIAN_POINT('',(32.5,-32.5,21.));
#9012=CARTESIAN_POINT('',(31.7928932188135,-31.7928932188135,20.));
#9013=CARTESIAN_POINT('Origin',(-47.5,-47.5,20.));
#9014=CARTESIAN_POINT('',(-45.,-50.,34.));
#9015=CARTESIAN_POINT('',(-45.,-50.,20.));
#9016=CARTESIAN_POINT('',(-50.,-45.,34.));
#9017=CARTESIAN_POINT('',(-47.5,-47.5,34.));
#9018=CARTESIAN_POINT('',(-50.,-45.,20.));
#9019=CARTESIAN_POINT('Origin',(-50.,-50.,20.));
#9020=CARTESIAN_POINT('',(25.,-50.,34.));
#9021=CARTESIAN_POINT('',(25.,-50.,20.));
#9022=CARTESIAN_POINT('',(-25.,-50.,34.));
#9023=CARTESIAN_POINT('Origin',(27.5,-47.5,20.));
#9024=CARTESIAN_POINT('',(30.,-45.,34.));
#9025=CARTESIAN_POINT('',(30.,-45.,20.));
#9026=CARTESIAN_POINT('',(32.5,-42.5,34.));
#9027=CARTESIAN_POINT('Origin',(30.,-50.,20.));
#9028=CARTESIAN_POINT('',(30.,-35.,34.));
#9029=CARTESIAN_POINT('',(30.,-35.,20.));
#9030=CARTESIAN_POINT('',(30.,-25.,34.));
#9031=CARTESIAN_POINT('Origin',(32.5,-32.5,20.));
#9032=CARTESIAN_POINT('',(35.,-30.,34.));
#9033=CARTESIAN_POINT('',(35.,-30.,20.));
#9034=CARTESIAN_POINT('',(32.5,-32.5,34.));
#9035=CARTESIAN_POINT('Origin',(30.,-30.,20.));
#9036=CARTESIAN_POINT('',(45.,-30.,34.));
#9037=CARTESIAN_POINT('',(45.,-30.,20.));
#9038=CARTESIAN_POINT('',(15.,-30.,34.));
#9039=CARTESIAN_POINT('Origin',(0.,0.,20.));
#9040=CARTESIAN_POINT('Origin',(29.,-25.,34.));
#9041=CARTESIAN_POINT('',(29.,-34.5857864376269,35.));
#9042=CARTESIAN_POINT('',(29.,-44.5857864376269,35.));
#9043=CARTESIAN_POINT('',(29.,-25.,35.));
#9044=CARTESIAN_POINT('Origin',(29.,-44.5857864376269,34.));
#9045=CARTESIAN_POINT('Origin',(29.,-34.5857864376269,34.));
#9046=CARTESIAN_POINT('Origin',(31.7928932188135,-41.7928932188135,34.));
#9047=CARTESIAN_POINT('',(24.5857864376269,-49.,35.));
#9048=CARTESIAN_POINT('',(31.7928932188135,-41.7928932188135,35.));
#9049=CARTESIAN_POINT('Origin',(24.5857864376269,-49.,34.));
#9050=CARTESIAN_POINT('Origin',(-25.,-49.,34.));
#9051=CARTESIAN_POINT('',(-44.5857864376269,-49.,35.));
#9052=CARTESIAN_POINT('',(-25.,-49.,35.));
#9053=CARTESIAN_POINT('Origin',(-44.5857864376269,-49.,34.));
#9054=CARTESIAN_POINT('Origin',(-46.7928932188135,-46.7928932188135,34.));
#9055=CARTESIAN_POINT('',(-49.,-44.5857864376269,35.));
#9056=CARTESIAN_POINT('',(-46.7928932188135,-46.7928932188135,35.));
#9057=CARTESIAN_POINT('Origin',(-49.,-44.5857864376269,34.));
#9058=CARTESIAN_POINT('Origin',(-49.,25.,34.));
#9059=CARTESIAN_POINT('',(-49.,44.5857864376269,35.));
#9060=CARTESIAN_POINT('',(-49.,25.,35.));
#9061=CARTESIAN_POINT('',(-50.,45.,34.));
#9062=CARTESIAN_POINT('Origin',(-49.,44.5857864376269,34.));
#9063=CARTESIAN_POINT('',(-50.,25.,34.));
#9064=CARTESIAN_POINT('Origin',(-46.7928932188135,46.7928932188135,34.));
#9065=CARTESIAN_POINT('',(-45.,50.,34.));
#9066=CARTESIAN_POINT('',(-47.5,47.5,34.));
#9067=CARTESIAN_POINT('',(-44.5857864376269,49.,35.));
#9068=CARTESIAN_POINT('',(-46.7928932188135,46.7928932188135,35.));
#9069=CARTESIAN_POINT('Origin',(-44.5857864376269,49.,34.));
#9070=CARTESIAN_POINT('Origin',(25.,49.,34.));
#9071=CARTESIAN_POINT('',(45.,50.,34.));
#9072=CARTESIAN_POINT('',(25.,50.,34.));
#9073=CARTESIAN_POINT('',(44.5857864376269,49.,35.));
#9074=CARTESIAN_POINT('',(25.,49.,35.));
#9075=CARTESIAN_POINT('Origin',(44.5857864376269,49.,34.));
#9076=CARTESIAN_POINT('Origin',(46.7928932188135,46.7928932188135,34.));
#9077=CARTESIAN_POINT('',(50.,45.,34.));
#9078=CARTESIAN_POINT('',(47.5,47.5,34.));
#9079=CARTESIAN_POINT('',(49.,44.5857864376269,35.));
#9080=CARTESIAN_POINT('',(46.7928932188135,46.7928932188135,35.));
#9081=CARTESIAN_POINT('Origin',(49.,44.5857864376269,34.));
#9082=CARTESIAN_POINT('Origin',(49.,-15.,34.));
#9083=CARTESIAN_POINT('',(50.,-25.,34.));
#9084=CARTESIAN_POINT('',(50.,-15.,34.));
#9085=CARTESIAN_POINT('',(49.,-24.5857864376269,35.));
#9086=CARTESIAN_POINT('',(49.,-15.,35.));
#9087=CARTESIAN_POINT('Origin',(49.,-24.5857864376269,34.));
#9088=CARTESIAN_POINT('Origin',(41.7928932188135,-31.7928932188135,34.));
#9089=CARTESIAN_POINT('',(42.5,-32.5,34.));
#9090=CARTESIAN_POINT('',(44.5857864376269,-29.,35.));
#9091=CARTESIAN_POINT('',(41.7928932188135,-31.7928932188135,35.));
#9092=CARTESIAN_POINT('Origin',(44.5857864376269,-29.,34.));
#9093=CARTESIAN_POINT('Origin',(15.,-29.,34.));
#9094=CARTESIAN_POINT('',(34.5857864376269,-29.,35.));
#9095=CARTESIAN_POINT('',(15.,-29.,35.));
#9096=CARTESIAN_POINT('Origin',(34.5857864376269,-29.,34.));
#9097=CARTESIAN_POINT('Origin',(31.7928932188135,-31.7928932188135,34.));
#9098=CARTESIAN_POINT('',(31.7928932188135,-31.7928932188135,35.));
#9099=CARTESIAN_POINT('Origin',(47.5,47.5,20.));
#9100=CARTESIAN_POINT('',(45.,50.,20.));
#9101=CARTESIAN_POINT('',(50.,45.,20.));
#9102=CARTESIAN_POINT('Origin',(50.,-30.,20.));
#9103=CARTESIAN_POINT('',(50.,-25.,20.));
#9104=CARTESIAN_POINT('Origin',(47.5,-27.5,20.));
#9105=CARTESIAN_POINT('Origin',(0.,0.,35.));
#9106=CARTESIAN_POINT('Origin',(-47.5,47.5,20.));
#9107=CARTESIAN_POINT('',(-50.,45.,20.));
#9108=CARTESIAN_POINT('',(-45.,50.,20.));
#9109=CARTESIAN_POINT('Origin',(50.,50.,20.));
#9110=CARTESIAN_POINT('Origin',(-50.,50.,20.));
#10112=UNCERTAINTY_MEASURE_WITH_UNIT(LENGTH_MEASURE(0.01),#10132,
'DISTANCE_ACCURACY_VALUE',
'Maximum model space distance between geometric entities at asserted c
onnectivities');
#10119=UNCERTAINTY_MEASURE_WITH_UNIT(LENGTH_MEASURE(0.01),#10132,
'DISTANCE_ACCURACY_VALUE',
'Maximum model space distance between geometric entities at asserted c
onnectivities');
#10124=(
GEOMETRIC_REPRESENTATION_CONTEXT(3)
GLOBAL_UNCERTAINTY_ASSIGNED_CONTEXT((#10112))
GLOBAL_UNIT_ASSIGNED_CONTEXT((#10132,#10134,#10135))
REPRESENTATION_CONTEXT('','3D')
);
#10131=(
GEOMETRIC_REPRESENTATION_CONTEXT(3)
GLOBAL_UNCERTAINTY_ASSIGNED_CONTEXT((#10119))
GLOBAL_UNIT_ASSIGNED_CONTEXT((#10132,#10134,#10135))
REPRESENTATION_CONTEXT('','3D')
);
#10132=(
LENGTH_UNIT()
NAMED_UNIT(*)
SI_UNIT(.MILLI.,.METRE.)
);
#10134=(
NAMED_UNIT(*)
PLANE_ANGLE_UNIT()
SI_UNIT($,.RADIAN.)
);
#10135=(
NAMED_UNIT(*)
SI_UNIT($,.STERADIAN.)
SOLID_ANGLE_UNIT()
);
#10140=SHAPE_DEFINITION_REPRESENTATION(#10151,#10172);
#10151=PRODUCT_DEFINITION_SHAPE('',$,#10184);
#10172=SHAPE_REPRESENTATION('',(#6173),#10124);
#10179=PRODUCT_DEFINITION_CONTEXT('part definition',#10214,'design');
#10184=PRODUCT_DEFINITION('Bottom_Block_01','Bottom_Block_01',#10195,#10179);
#10195=PRODUCT_DEFINITION_FORMATION('',$,#10220);
#10214=APPLICATION_CONTEXT(
'Core Data for Automotive Mechanical Design Process');
#10215=PRODUCT_CONTEXT('part definition',#10214,'mechanical');
#10220=PRODUCT('Bottom_Block_01','Bottom_Block_01',$,(#10215));
#10241=COLOUR_RGB('Dark Blue',0.08,0.2,0.34);
#10242=FILL_AREA_STYLE_COLOUR('',#10241);
#10243=FILL_AREA_STYLE('',(#10242));
#10244=SURFACE_STYLE_FILL_AREA(#10243);
#10245=SURFACE_SIDE_STYLE('',(#10244));
#10246=SURFACE_STYLE_USAGE(.BOTH.,#10245);
#10247=PRESENTATION_STYLE_ASSIGNMENT((#10246));
ENDSEC;
END-ISO-10303-21;
